ISO-10303-21;
HEADER;
/* Generated by software containing ST-Developer
 * from STEP Tools, Inc. (www.steptools.com) 
 */

FILE_DESCRIPTION(
/* description */ ('Union bypass pipe loop'),
/* implementation_level */ '2;1');

FILE_NAME(
/* name */ 'Flat Washer - M5.step',
/* time_stamp */ '2026-10-27T21:00:29-07:00',
/* author */ (''),
/* organization */ (''),
/* preprocessor_version */ 'ST-DEVELOPER v20.2',
/* originating_system */ 'Autodesk Translation Framework v15.17.0.0',
/* authorisation */ '');

FILE_SCHEMA (('AUTOMOTIVE_DESIGN { 1 0 10303 214 3 1 1 }'));
ENDSEC;

DATA;
#10=MECHANICAL_DESIGN_GEOMETRIC_PRESENTATION_REPRESENTATION('',(#454),#10095);
#354=CONICAL_SURFACE('',#6121,0.275,0.785398163397449);
#390=SHAPE_REPRESENTATION_RELATIONSHIP('SRR','None',#10259,#422);
#422=ADVANCED_BREP_SHAPE_REPRESENTATION('',(#485),#10071);
#454=STYLED_ITEM('',(#10507),#485);
#485=MANIFOLD_SOLID_BREP('Body1',#5526);
#570=FACE_BOUND('',#1338,.T.);
#571=FACE_BOUND('',#1341,.T.);
#696=PLANE('',#6126);
#697=PLANE('',#6130);
#944=FACE_OUTER_BOUND('',#1335,.T.);
#945=FACE_OUTER_BOUND('',#1336,.T.);
#946=FACE_OUTER_BOUND('',#1337,.T.);
#947=FACE_OUTER_BOUND('',#1339,.T.);
#948=FACE_OUTER_BOUND('',#1340,.T.);
#1335=EDGE_LOOP('',(#4192,#4193,#4194,#4195));
#1336=EDGE_LOOP('',(#4196,#4197,#4198,#4199));
#1337=EDGE_LOOP('',(#4200));
#1338=EDGE_LOOP('',(#4201));
#1339=EDGE_LOOP('',(#4202,#4203,#4204,#4205));
#1340=EDGE_LOOP('',(#4206));
#1341=EDGE_LOOP('',(#4207));
#1756=LINE('',#8927,#2132);
#1757=LINE('',#8931,#2133);
#1758=LINE('',#8938,#2134);
#2132=VECTOR('',#7188,0.275);
#2133=VECTOR('',#7193,0.265);
#2134=VECTOR('',#7202,0.5);
#2469=CIRCLE('',#6122,0.285);
#2470=CIRCLE('',#6123,0.265);
#2471=CIRCLE('',#6125,0.265);
#2472=CIRCLE('',#6127,0.5);
#2473=CIRCLE('',#6129,0.5);
#2781=VERTEX_POINT('',#8924);
#2782=VERTEX_POINT('',#8926);
#2783=VERTEX_POINT('',#8930);
#2784=VERTEX_POINT('',#8934);
#2785=VERTEX_POINT('',#8937);
#3294=EDGE_CURVE('',#2781,#2781,#2469,.T.);
#3295=EDGE_CURVE('',#2781,#2782,#1756,.T.);
#3296=EDGE_CURVE('',#2782,#2782,#2470,.T.);
#3297=EDGE_CURVE('',#2782,#2783,#1757,.T.);
#3298=EDGE_CURVE('',#2783,#2783,#2471,.T.);
#3299=EDGE_CURVE('',#2784,#2784,#2472,.T.);
#3300=EDGE_CURVE('',#2784,#2785,#1758,.T.);
#3301=EDGE_CURVE('',#2785,#2785,#2473,.T.);
#4192=ORIENTED_EDGE('',*,*,#3294,.T.);
#4193=ORIENTED_EDGE('',*,*,#3295,.T.);
#4194=ORIENTED_EDGE('',*,*,#3296,.T.);
#4195=ORIENTED_EDGE('',*,*,#3295,.F.);
#4196=ORIENTED_EDGE('',*,*,#3296,.F.);
#4197=ORIENTED_EDGE('',*,*,#3297,.T.);
#4198=ORIENTED_EDGE('',*,*,#3298,.T.);
#4199=ORIENTED_EDGE('',*,*,#3297,.F.);
#4200=ORIENTED_EDGE('',*,*,#3299,.T.);
#4201=ORIENTED_EDGE('',*,*,#3294,.F.);
#4202=ORIENTED_EDGE('',*,*,#3299,.F.);
#4203=ORIENTED_EDGE('',*,*,#3300,.T.);
#4204=ORIENTED_EDGE('',*,*,#3301,.T.);
#4205=ORIENTED_EDGE('',*,*,#3300,.F.);
#4206=ORIENTED_EDGE('',*,*,#3301,.F.);
#4207=ORIENTED_EDGE('',*,*,#3298,.F.);
#5121=CYLINDRICAL_SURFACE('',#6124,0.265);
#5122=CYLINDRICAL_SURFACE('',#6128,0.5);
#5293=ADVANCED_FACE('',(#944),#354,.F.);
#5294=ADVANCED_FACE('',(#945),#5121,.F.);
#5295=ADVANCED_FACE('',(#946,#570),#696,.T.);
#5296=ADVANCED_FACE('',(#947),#5122,.T.);
#5297=ADVANCED_FACE('',(#948,#571),#697,.F.);
#5526=CLOSED_SHELL('',(#5293,#5294,#5295,#5296,#5297));
#6120=AXIS2_PLACEMENT_3D('',#8922,#7182,#7183);
#6121=AXIS2_PLACEMENT_3D('',#8923,#7184,#7185);
#6122=AXIS2_PLACEMENT_3D('',#8925,#7186,#7187);
#6123=AXIS2_PLACEMENT_3D('',#8928,#7189,#7190);
#6124=AXIS2_PLACEMENT_3D('',#8929,#7191,#7192);
#6125=AXIS2_PLACEMENT_3D('',#8932,#7194,#7195);
#6126=AXIS2_PLACEMENT_3D('',#8933,#7196,#7197);
#6127=AXIS2_PLACEMENT_3D('',#8935,#7198,#7199);
#6128=AXIS2_PLACEMENT_3D('',#8936,#7200,#7201);
#6129=AXIS2_PLACEMENT_3D('',#8939,#7203,#7204);
#6130=AXIS2_PLACEMENT_3D('',#8940,#7205,#7206);
#7182=DIRECTION('axis',(0.,0.,1.));
#7183=DIRECTION('refdir',(1.,0.,0.));
#7184=DIRECTION('center_axis',(0.,1.,0.));
#7185=DIRECTION('ref_axis',(1.,0.,0.));
#7186=DIRECTION('center_axis',(0.,1.,0.));
#7187=DIRECTION('ref_axis',(1.,0.,0.));
#7188=DIRECTION('',(0.707106781186548,-0.707106781186547,-8.65956056235494E-17));
#7189=DIRECTION('center_axis',(0.,-1.,0.));
#7190=DIRECTION('ref_axis',(1.,0.,0.));
#7191=DIRECTION('center_axis',(0.,1.,0.));
#7192=DIRECTION('ref_axis',(1.,0.,0.));
#7193=DIRECTION('',(0.,-1.,0.));
#7194=DIRECTION('center_axis',(0.,-1.,0.));
#7195=DIRECTION('ref_axis',(1.,0.,0.));
#7196=DIRECTION('center_axis',(0.,1.,0.));
#7197=DIRECTION('ref_axis',(1.,0.,0.));
#7198=DIRECTION('center_axis',(0.,1.,0.));
#7199=DIRECTION('ref_axis',(1.,0.,0.));
#7200=DIRECTION('center_axis',(0.,1.,0.));
#7201=DIRECTION('ref_axis',(1.,0.,0.));
#7202=DIRECTION('',(0.,-1.,0.));
#7203=DIRECTION('center_axis',(0.,1.,0.));
#7204=DIRECTION('ref_axis',(1.,0.,0.));
#7205=DIRECTION('center_axis',(0.,1.,0.));
#7206=DIRECTION('ref_axis',(1.,0.,0.));
#8922=CARTESIAN_POINT('',(0.,0.,0.));
#8923=CARTESIAN_POINT('Origin',(0.,0.09,0.));
#8924=CARTESIAN_POINT('',(-0.285,0.1,3.49024337756996E-17));
#8925=CARTESIAN_POINT('Origin',(0.,0.1,0.));
#8926=CARTESIAN_POINT('',(-0.265,0.08,-3.24531401774049E-17));
#8927=CARTESIAN_POINT('',(-0.275,0.09,3.36777869765522E-17));
#8928=CARTESIAN_POINT('Origin',(0.,0.08,0.));
#8929=CARTESIAN_POINT('Origin',(0.,0.,0.));
#8930=CARTESIAN_POINT('',(-0.265,0.,3.24531401774049E-17));
#8931=CARTESIAN_POINT('',(-0.265,0.,3.24531401774049E-17));
#8932=CARTESIAN_POINT('Origin',(0.,0.,0.));
#8933=CARTESIAN_POINT('Origin',(0.,0.1,0.));
#8934=CARTESIAN_POINT('',(-0.5,0.1,6.12323399573677E-17));
#8935=CARTESIAN_POINT('Origin',(0.,0.1,0.));
#8936=CARTESIAN_POINT('Origin',(0.,0.,0.));
#8937=CARTESIAN_POINT('',(-0.5,0.,6.12323399573677E-17));
#8938=CARTESIAN_POINT('',(-0.5,0.,6.12323399573677E-17));
#8939=CARTESIAN_POINT('Origin',(0.,0.,0.));
#8940=CARTESIAN_POINT('Origin',(0.,0.,0.));
#10034=UNCERTAINTY_MEASURE_WITH_UNIT(LENGTH_MEASURE(0.001),#10096,
'DISTANCE_ACCURACY_VALUE',
'Maximum model space distance between geometric entities at asserted c
onnectivities');
#10058=UNCERTAINTY_MEASURE_WITH_UNIT(LENGTH_MEASURE(0.001),#10096,
'DISTANCE_ACCURACY_VALUE',
'Maximum model space distance between geometric entities at asserted c
onnectivities');
#10071=(
GEOMETRIC_REPRESENTATION_CONTEXT(3)
GLOBAL_UNCERTAINTY_ASSIGNED_CONTEXT((#10034))
GLOBAL_UNIT_ASSIGNED_CONTEXT((#10096,#10098,#10099))
REPRESENTATION_CONTEXT('','3D')
);
#10095=(
GEOMETRIC_REPRESENTATION_CONTEXT(3)
GLOBAL_UNCERTAINTY_ASSIGNED_CONTEXT((#10058))
GLOBAL_UNIT_ASSIGNED_CONTEXT((#10096,#10098,#10099))
REPRESENTATION_CONTEXT('','3D')
);
#10096=(
LENGTH_UNIT()
NAMED_UNIT(*)
SI_UNIT(.CENTI.,.METRE.)
);
#10098=(
NAMED_UNIT(*)
PLANE_ANGLE_UNIT()
SI_UNIT($,.RADIAN.)
);
#10099=(
NAMED_UNIT(*)
SI_UNIT($,.STERADIAN.)
SOLID_ANGLE_UNIT()
);
#10112=SHAPE_DEFINITION_REPRESENTATION(#10148,#10259);
#10148=PRODUCT_DEFINITION_SHAPE('',$,#10296);
#10259=SHAPE_REPRESENTATION('',(#6120),#10071);
#10283=PRODUCT_DEFINITION_CONTEXT('part definition',#10393,'design');
#10296=PRODUCT_DEFINITION('Flat Washer - M5','Flat Washer - M5',#10332,
#10283);
#10332=PRODUCT_DEFINITION_FORMATION('',$,#10407);
#10393=APPLICATION_CONTEXT(
'Core Data for Automotive Mechanical Design Process');
#10394=PRODUCT_CONTEXT('part definition',#10393,'mechanical');
#10407=PRODUCT('Flat Washer - M5','Flat Washer - M5','Flat Washer - M5',
(#10394));
#10501=COLOUR_RGB('Black',0.12,0.14,0.17);
#10502=FILL_AREA_STYLE_COLOUR('',#10501);
#10503=FILL_AREA_STYLE('',(#10502));
#10504=SURFACE_STYLE_FILL_AREA(#10503);
#10505=SURFACE_SIDE_STYLE('',(#10504));
#10506=SURFACE_STYLE_USAGE(.BOTH.,#10505);
#10507=PRESENTATION_STYLE_ASSIGNMENT((#10506));
ENDSEC;
END-ISO-10303-21;
